ISO-10303-21;
HEADER;
/* Generated by software containing ST-Developer
 * from STEP Tools, Inc. (www.steptools.com) 
 */

FILE_DESCRIPTION(
/* description */ ('Independent equipment support assembly with bolted 600 x 500 mm welde
d perimeter frame, four adjustable legs and swivel feet. Nominal overa
ll height 518 mm. No load rating assigned.'),
/* implementation_level */ '2;1');

FILE_NAME(
/* name */ 'Flat washer M10.step',
/* time_stamp */ '2026-11-07T17:30:39-08:00',
/* author */ (''),
/* organization */ (''),
/* preprocessor_version */ 'ST-DEVELOPER v20.2',
/* originating_system */ 'Autodesk Translation Framework v15.17.0.0',
/* authorisation */ '');

FILE_SCHEMA (('AUTOMOTIVE_DESIGN { 1 0 10303 214 3 1 1 }'));
ENDSEC;

DATA;
#10=MECHANICAL_DESIGN_GEOMETRIC_PRESENTATION_REPRESENTATION('',(#2221),#63755);
#472=CIRCLE('',#15427,5.5);
#473=CIRCLE('',#15428,5.5);
#474=CIRCLE('',#15430,11.);
#475=CIRCLE('',#15431,11.);
#2139=CYLINDRICAL_SURFACE('',#15426,5.5);
#2140=CYLINDRICAL_SURFACE('',#15429,11.);
#2189=SHAPE_REPRESENTATION_RELATIONSHIP('SRR','None',#63874,#2205);
#2205=ADVANCED_BREP_SHAPE_REPRESENTATION('',(#2237),#63752);
#2221=STYLED_ITEM('',(#63961),#2237);
#2237=MANIFOLD_SOLID_BREP('Body1',#14322);
#2297=FACE_BOUND('',#3829,.T.);
#2298=FACE_BOUND('',#3831,.T.);
#3009=FACE_OUTER_BOUND('',#3826,.T.);
#3010=FACE_OUTER_BOUND('',#3827,.T.);
#3011=FACE_OUTER_BOUND('',#3828,.T.);
#3012=FACE_OUTER_BOUND('',#3830,.T.);
#3826=EDGE_LOOP('',(#13133,#13134,#13135,#13136));
#3827=EDGE_LOOP('',(#13137,#13138,#13139,#13140));
#3828=EDGE_LOOP('',(#13141));
#3829=EDGE_LOOP('',(#13142));
#3830=EDGE_LOOP('',(#13143));
#3831=EDGE_LOOP('',(#13144));
#4668=LINE('',#61148,#5504);
#4669=LINE('',#61154,#5505);
#5504=VECTOR('',#18149,5.5);
#5505=VECTOR('',#18156,11.);
#6894=VERTEX_POINT('',#61145);
#6895=VERTEX_POINT('',#61147);
#6896=VERTEX_POINT('',#61151);
#6897=VERTEX_POINT('',#61153);
#8989=EDGE_CURVE('',#6894,#6894,#472,.T.);
#8990=EDGE_CURVE('',#6894,#6895,#4668,.T.);
#8991=EDGE_CURVE('',#6895,#6895,#473,.T.);
#8992=EDGE_CURVE('',#6896,#6896,#474,.T.);
#8993=EDGE_CURVE('',#6896,#6897,#4669,.T.);
#8994=EDGE_CURVE('',#6897,#6897,#475,.T.);
#13133=ORIENTED_EDGE('',*,*,#8989,.F.);
#13134=ORIENTED_EDGE('',*,*,#8990,.T.);
#13135=ORIENTED_EDGE('',*,*,#8991,.T.);
#13136=ORIENTED_EDGE('',*,*,#8990,.F.);
#13137=ORIENTED_EDGE('',*,*,#8992,.F.);
#13138=ORIENTED_EDGE('',*,*,#8993,.T.);
#13139=ORIENTED_EDGE('',*,*,#8994,.T.);
#13140=ORIENTED_EDGE('',*,*,#8993,.F.);
#13141=ORIENTED_EDGE('',*,*,#8992,.T.);
#13142=ORIENTED_EDGE('',*,*,#8989,.T.);
#13143=ORIENTED_EDGE('',*,*,#8994,.F.);
#13144=ORIENTED_EDGE('',*,*,#8991,.F.);
#13535=PLANE('',#15432);
#13536=PLANE('',#15433);
#14255=ADVANCED_FACE('',(#3009),#2139,.F.);
#14256=ADVANCED_FACE('',(#3010),#2140,.T.);
#14257=ADVANCED_FACE('',(#3011,#2297),#13535,.T.);
#14258=ADVANCED_FACE('',(#3012,#2298),#13536,.F.);
#14322=CLOSED_SHELL('',(#14255,#14256,#14257,#14258));
#15425=AXIS2_PLACEMENT_3D('',#61143,#18143,#18144);
#15426=AXIS2_PLACEMENT_3D('',#61144,#18145,#18146);
#15427=AXIS2_PLACEMENT_3D('',#61146,#18147,#18148);
#15428=AXIS2_PLACEMENT_3D('',#61149,#18150,#18151);
#15429=AXIS2_PLACEMENT_3D('',#61150,#18152,#18153);
#15430=AXIS2_PLACEMENT_3D('',#61152,#18154,#18155);
#15431=AXIS2_PLACEMENT_3D('',#61155,#18157,#18158);
#15432=AXIS2_PLACEMENT_3D('',#61156,#18159,#18160);
#15433=AXIS2_PLACEMENT_3D('',#61157,#18161,#18162);
#18143=DIRECTION('axis',(0.,0.,1.));
#18144=DIRECTION('refdir',(1.,0.,0.));
#18145=DIRECTION('center_axis',(0.,0.,1.));
#18146=DIRECTION('ref_axis',(1.,0.,0.));
#18147=DIRECTION('center_axis',(0.,0.,-1.));
#18148=DIRECTION('ref_axis',(1.,0.,0.));
#18149=DIRECTION('',(0.,0.,-1.));
#18150=DIRECTION('center_axis',(0.,0.,-1.));
#18151=DIRECTION('ref_axis',(1.,0.,0.));
#18152=DIRECTION('center_axis',(0.,0.,1.));
#18153=DIRECTION('ref_axis',(1.,0.,0.));
#18154=DIRECTION('center_axis',(0.,0.,1.));
#18155=DIRECTION('ref_axis',(1.,0.,0.));
#18156=DIRECTION('',(0.,0.,-1.));
#18157=DIRECTION('center_axis',(0.,0.,1.));
#18158=DIRECTION('ref_axis',(1.,0.,0.));
#18159=DIRECTION('center_axis',(0.,0.,1.));
#18160=DIRECTION('ref_axis',(1.,0.,0.));
#18161=DIRECTION('center_axis',(0.,0.,1.));
#18162=DIRECTION('ref_axis',(1.,0.,0.));
#61143=CARTESIAN_POINT('',(0.,0.,0.));
#61144=CARTESIAN_POINT('Origin',(0.,0.,0.));
#61145=CARTESIAN_POINT('',(-5.5,-6.73555739531044E-16,2.));
#61146=CARTESIAN_POINT('Origin',(0.,0.,2.));
#61147=CARTESIAN_POINT('',(-5.5,-6.73555739531044E-16,0.));
#61148=CARTESIAN_POINT('',(-5.5,-6.73555739531044E-16,0.));
#61149=CARTESIAN_POINT('Origin',(0.,0.,0.));
#61150=CARTESIAN_POINT('Origin',(0.,0.,0.));
#61151=CARTESIAN_POINT('',(-11.,-1.34711147906209E-15,2.));
#61152=CARTESIAN_POINT('Origin',(0.,0.,2.));
#61153=CARTESIAN_POINT('',(-11.,-1.34711147906209E-15,0.));
#61154=CARTESIAN_POINT('',(-11.,-1.34711147906209E-15,0.));
#61155=CARTESIAN_POINT('Origin',(0.,0.,0.));
#61156=CARTESIAN_POINT('Origin',(0.,0.,2.));
#61157=CARTESIAN_POINT('Origin',(0.,0.,0.));
#63732=UNCERTAINTY_MEASURE_WITH_UNIT(LENGTH_MEASURE(0.01),#63756,
'DISTANCE_ACCURACY_VALUE',
'Maximum model space distance between geometric entities at asserted c
onnectivities');
#63735=UNCERTAINTY_MEASURE_WITH_UNIT(LENGTH_MEASURE(0.01),#63756,
'DISTANCE_ACCURACY_VALUE',
'Maximum model space distance between geometric entities at asserted c
onnectivities');
#63752=(
GEOMETRIC_REPRESENTATION_CONTEXT(3)
GLOBAL_UNCERTAINTY_ASSIGNED_CONTEXT((#63732))
GLOBAL_UNIT_ASSIGNED_CONTEXT((#63756,#63758,#63759))
REPRESENTATION_CONTEXT('','3D')
);
#63755=(
GEOMETRIC_REPRESENTATION_CONTEXT(3)
GLOBAL_UNCERTAINTY_ASSIGNED_CONTEXT((#63735))
GLOBAL_UNIT_ASSIGNED_CONTEXT((#63756,#63758,#63759))
REPRESENTATION_CONTEXT('','3D')
);
#63756=(
LENGTH_UNIT()
NAMED_UNIT(*)
SI_UNIT(.MILLI.,.METRE.)
);
#63758=(
NAMED_UNIT(*)
PLANE_ANGLE_UNIT()
SI_UNIT($,.RADIAN.)
);
#63759=(
NAMED_UNIT(*)
SI_UNIT($,.STERADIAN.)
SOLID_ANGLE_UNIT()
);
#63776=SHAPE_DEFINITION_REPRESENTATION(#63835,#63874);
#63835=PRODUCT_DEFINITION_SHAPE('',$,#63894);
#63874=SHAPE_REPRESENTATION('',(#15425),#63752);
#63877=PRODUCT_DEFINITION_CONTEXT('part definition',#63936,'design');
#63894=PRODUCT_DEFINITION('Flat washer M10','Flat washer M10',#63913,#63877);
#63913=PRODUCT_DEFINITION_FORMATION('',$,#63954);
#63936=APPLICATION_CONTEXT(
'Core Data for Automotive Mechanical Design Process');
#63937=PRODUCT_CONTEXT('part definition',#63936,'mechanical');
#63954=PRODUCT('Flat washer M10','Flat washer M10',$,(#63937));
#63961=PRESENTATION_STYLE_ASSIGNMENT((#63968));
#63968=SURFACE_STYLE_USAGE(.BOTH.,#63975);
#63975=SURFACE_SIDE_STYLE('',(#63982));
#63982=SURFACE_STYLE_FILL_AREA(#63989);
#63989=FILL_AREA_STYLE('Light gray',(#63996));
#63996=FILL_AREA_STYLE_COLOUR('Light gray',#64003);
#64003=COLOUR_RGB('Light gray',0.725490196078431,0.752941176470588,0.792156862745098);
ENDSEC;
END-ISO-10303-21;
